ISO-10303-21;
HEADER;
/* Generated by software containing ST-Developer
 * from STEP Tools, Inc. (www.steptools.com) 
 */

FILE_DESCRIPTION(
/* description */ ('PAT-091'),
/* implementation_level */ '2;1');

FILE_NAME(
/* name */ 'Screw retaining collar (1).step',
/* time_stamp */ '2026-10-27T15:34:44-07:00',
/* author */ (''),
/* organization */ (''),
/* preprocessor_version */ 'ST-DEVELOPER v20.2',
/* originating_system */ 'Autodesk Translation Framework v15.17.0.0',
/* authorisation */ '');

FILE_SCHEMA (('AUTOMOTIVE_DESIGN { 1 0 10303 214 3 1 1 }'));
ENDSEC;

DATA;
#10=MECHANICAL_DESIGN_GEOMETRIC_PRESENTATION_REPRESENTATION('',(#1092),#25100);
#859=SHAPE_REPRESENTATION_RELATIONSHIP('SRR','None',#25628,#969);
#969=ADVANCED_BREP_SHAPE_REPRESENTATION('',(#1213),#25098);
#1092=STYLED_ITEM('',(#26198),#1213);
#1213=MANIFOLD_SOLID_BREP('Body1',#13372);
#1635=FACE_BOUND('',#4112,.T.);
#1636=FACE_BOUND('',#4114,.T.);
#2058=PLANE('',#16439);
#2059=PLANE('',#16440);
#2871=FACE_OUTER_BOUND('',#4109,.T.);
#2872=FACE_OUTER_BOUND('',#4110,.T.);
#2873=FACE_OUTER_BOUND('',#4111,.T.);
#2874=FACE_OUTER_BOUND('',#4113,.T.);
#4109=EDGE_LOOP('',(#12044,#12045,#12046,#12047));
#4110=EDGE_LOOP('',(#12048,#12049,#12050,#12051));
#4111=EDGE_LOOP('',(#12052));
#4112=EDGE_LOOP('',(#12053));
#4113=EDGE_LOOP('',(#12054));
#4114=EDGE_LOOP('',(#12055));
#4859=LINE('',#24813,#5599);
#4860=LINE('',#24819,#5600);
#5599=VECTOR('',#20903,0.6);
#5600=VECTOR('',#20910,0.9);
#6373=CIRCLE('',#16434,0.6);
#6374=CIRCLE('',#16435,0.6);
#6375=CIRCLE('',#16437,0.9);
#6376=CIRCLE('',#16438,0.9);
#7411=VERTEX_POINT('',#24810);
#7412=VERTEX_POINT('',#24812);
#7413=VERTEX_POINT('',#24816);
#7414=VERTEX_POINT('',#24818);
#8957=EDGE_CURVE('',#7411,#7411,#6373,.T.);
#8958=EDGE_CURVE('',#7411,#7412,#4859,.T.);
#8959=EDGE_CURVE('',#7412,#7412,#6374,.T.);
#8960=EDGE_CURVE('',#7413,#7413,#6375,.T.);
#8961=EDGE_CURVE('',#7413,#7414,#4860,.T.);
#8962=EDGE_CURVE('',#7414,#7414,#6376,.T.);
#12044=ORIENTED_EDGE('',*,*,#8957,.F.);
#12045=ORIENTED_EDGE('',*,*,#8958,.T.);
#12046=ORIENTED_EDGE('',*,*,#8959,.T.);
#12047=ORIENTED_EDGE('',*,*,#8958,.F.);
#12048=ORIENTED_EDGE('',*,*,#8960,.F.);
#12049=ORIENTED_EDGE('',*,*,#8961,.T.);
#12050=ORIENTED_EDGE('',*,*,#8962,.T.);
#12051=ORIENTED_EDGE('',*,*,#8961,.F.);
#12052=ORIENTED_EDGE('',*,*,#8960,.T.);
#12053=ORIENTED_EDGE('',*,*,#8957,.T.);
#12054=ORIENTED_EDGE('',*,*,#8962,.F.);
#12055=ORIENTED_EDGE('',*,*,#8959,.F.);
#12425=CYLINDRICAL_SURFACE('',#16433,0.6);
#12426=CYLINDRICAL_SURFACE('',#16436,0.9);
#13238=ADVANCED_FACE('',(#2871),#12425,.F.);
#13239=ADVANCED_FACE('',(#2872),#12426,.T.);
#13240=ADVANCED_FACE('',(#2873,#1635),#2058,.T.);
#13241=ADVANCED_FACE('',(#2874,#1636),#2059,.F.);
#13372=CLOSED_SHELL('',(#13238,#13239,#13240,#13241));
#16432=AXIS2_PLACEMENT_3D('',#24808,#20897,#20898);
#16433=AXIS2_PLACEMENT_3D('',#24809,#20899,#20900);
#16434=AXIS2_PLACEMENT_3D('',#24811,#20901,#20902);
#16435=AXIS2_PLACEMENT_3D('',#24814,#20904,#20905);
#16436=AXIS2_PLACEMENT_3D('',#24815,#20906,#20907);
#16437=AXIS2_PLACEMENT_3D('',#24817,#20908,#20909);
#16438=AXIS2_PLACEMENT_3D('',#24820,#20911,#20912);
#16439=AXIS2_PLACEMENT_3D('',#24821,#20913,#20914);
#16440=AXIS2_PLACEMENT_3D('',#24822,#20915,#20916);
#20897=DIRECTION('axis',(0.,0.,1.));
#20898=DIRECTION('refdir',(1.,0.,0.));
#20899=DIRECTION('center_axis',(1.,0.,0.));
#20900=DIRECTION('ref_axis',(0.,0.,-1.));
#20901=DIRECTION('center_axis',(-1.,0.,0.));
#20902=DIRECTION('ref_axis',(0.,0.,-1.));
#20903=DIRECTION('',(-1.,0.,0.));
#20904=DIRECTION('center_axis',(-1.,0.,0.));
#20905=DIRECTION('ref_axis',(0.,0.,-1.));
#20906=DIRECTION('center_axis',(1.,0.,0.));
#20907=DIRECTION('ref_axis',(0.,0.,-1.));
#20908=DIRECTION('center_axis',(1.,0.,0.));
#20909=DIRECTION('ref_axis',(0.,0.,-1.));
#20910=DIRECTION('',(-1.,0.,0.));
#20911=DIRECTION('center_axis',(1.,0.,0.));
#20912=DIRECTION('ref_axis',(0.,0.,-1.));
#20913=DIRECTION('center_axis',(1.,0.,0.));
#20914=DIRECTION('ref_axis',(0.,0.,-1.));
#20915=DIRECTION('center_axis',(1.,0.,0.));
#20916=DIRECTION('ref_axis',(0.,0.,-1.));
#24808=CARTESIAN_POINT('',(0.,0.,0.));
#24809=CARTESIAN_POINT('Origin',(46.3,0.,6.));
#24810=CARTESIAN_POINT('',(46.5,-7.34788079488412E-17,6.6));
#24811=CARTESIAN_POINT('Origin',(46.5,0.,6.));
#24812=CARTESIAN_POINT('',(46.3,-7.34788079488412E-17,6.6));
#24813=CARTESIAN_POINT('',(46.3,-7.34788079488412E-17,6.6));
#24814=CARTESIAN_POINT('Origin',(46.3,0.,6.));
#24815=CARTESIAN_POINT('Origin',(46.3,0.,6.));
#24816=CARTESIAN_POINT('',(46.5,-1.10218211923262E-16,6.9));
#24817=CARTESIAN_POINT('Origin',(46.5,0.,6.));
#24818=CARTESIAN_POINT('',(46.3,-1.10218211923262E-16,6.9));
#24819=CARTESIAN_POINT('',(46.3,-1.10218211923262E-16,6.9));
#24820=CARTESIAN_POINT('Origin',(46.3,0.,6.));
#24821=CARTESIAN_POINT('Origin',(46.5,0.,6.));
#24822=CARTESIAN_POINT('Origin',(46.3,0.,6.));
#24977=UNCERTAINTY_MEASURE_WITH_UNIT(LENGTH_MEASURE(0.001),#25101,
'DISTANCE_ACCURACY_VALUE',
'Maximum model space distance between geometric entities at asserted c
onnectivities');
#24979=UNCERTAINTY_MEASURE_WITH_UNIT(LENGTH_MEASURE(0.001),#25101,
'DISTANCE_ACCURACY_VALUE',
'Maximum model space distance between geometric entities at asserted c
onnectivities');
#25098=(
GEOMETRIC_REPRESENTATION_CONTEXT(3)
GLOBAL_UNCERTAINTY_ASSIGNED_CONTEXT((#24977))
GLOBAL_UNIT_ASSIGNED_CONTEXT((#25101,#25103,#25104))
REPRESENTATION_CONTEXT('','3D')
);
#25100=(
GEOMETRIC_REPRESENTATION_CONTEXT(3)
GLOBAL_UNCERTAINTY_ASSIGNED_CONTEXT((#24979))
GLOBAL_UNIT_ASSIGNED_CONTEXT((#25101,#25103,#25104))
REPRESENTATION_CONTEXT('','3D')
);
#25101=(
LENGTH_UNIT()
NAMED_UNIT(*)
SI_UNIT(.CENTI.,.METRE.)
);
#25103=(
NAMED_UNIT(*)
PLANE_ANGLE_UNIT()
SI_UNIT($,.RADIAN.)
);
#25104=(
NAMED_UNIT(*)
SI_UNIT($,.STERADIAN.)
SOLID_ANGLE_UNIT()
);
#25223=SHAPE_DEFINITION_REPRESENTATION(#25495,#25628);
#25495=PRODUCT_DEFINITION_SHAPE('',$,#25749);
#25628=SHAPE_REPRESENTATION('',(#16432),#25098);
#25630=PRODUCT_DEFINITION_CONTEXT('part definition',#25992,'design');
#25749=PRODUCT_DEFINITION('Screw retaining collar (1)',
'Screw retaining collar (1)',#25869,#25630);
#25869=PRODUCT_DEFINITION_FORMATION('',$,#26112);
#25992=APPLICATION_CONTEXT(
'Core Data for Automotive Mechanical Design Process');
#25993=PRODUCT_CONTEXT('part definition',#25992,'mechanical');
#26112=PRODUCT('Screw retaining collar (1)','Screw retaining collar (1)',
'Screw retaining collar (1)',(#25993));
#26192=COLOUR_RGB('Black',0.12,0.14,0.17);
#26193=FILL_AREA_STYLE_COLOUR('',#26192);
#26194=FILL_AREA_STYLE('',(#26193));
#26195=SURFACE_STYLE_FILL_AREA(#26194);
#26196=SURFACE_SIDE_STYLE('',(#26195));
#26197=SURFACE_STYLE_USAGE(.BOTH.,#26196);
#26198=PRESENTATION_STYLE_ASSIGNMENT((#26197));
ENDSEC;
END-ISO-10303-21;
